ISO-10303-21;
HEADER;
/* Generated by software containing ST-Developer
 * from STEP Tools, Inc. (www.steptools.com) 
 */

FILE_DESCRIPTION(
/* description */ ('Dual-rail gantry carriage'),
/* implementation_level */ '2;1');

FILE_NAME(
/* name */ 'Flat Washer - M6.step',
/* time_stamp */ '2026-10-27T10:49:15-07:00',
/* author */ (''),
/* organization */ (''),
/* preprocessor_version */ 'ST-DEVELOPER v20.2',
/* originating_system */ 'Autodesk Translation Framework v15.17.0.0',
/* authorisation */ '');

FILE_SCHEMA (('AUTOMOTIVE_DESIGN { 1 0 10303 214 3 1 1 }'));
ENDSEC;

DATA;
#10=MECHANICAL_DESIGN_GEOMETRIC_PRESENTATION_REPRESENTATION('',(#612),#12804);
#550=SHAPE_REPRESENTATION_RELATIONSHIP('SRR','None',#13030,#581);
#581=ADVANCED_BREP_SHAPE_REPRESENTATION('',(#640),#12800);
#612=STYLED_ITEM('',(#13254),#640);
#640=MANIFOLD_SOLID_BREP('Body1',#7393);
#758=FACE_BOUND('',#1903,.T.);
#759=FACE_BOUND('',#1905,.T.);
#1022=PLANE('',#8377);
#1023=PLANE('',#8378);
#1395=FACE_OUTER_BOUND('',#1900,.T.);
#1396=FACE_OUTER_BOUND('',#1901,.T.);
#1397=FACE_OUTER_BOUND('',#1902,.T.);
#1398=FACE_OUTER_BOUND('',#1904,.T.);
#1900=EDGE_LOOP('',(#6737,#6738,#6739,#6740));
#1901=EDGE_LOOP('',(#6741,#6742,#6743,#6744));
#1902=EDGE_LOOP('',(#6745));
#1903=EDGE_LOOP('',(#6746));
#1904=EDGE_LOOP('',(#6747));
#1905=EDGE_LOOP('',(#6748));
#2605=LINE('',#12521,#3314);
#2606=LINE('',#12527,#3315);
#3314=VECTOR('',#10408,0.32);
#3315=VECTOR('',#10415,0.6);
#3542=CIRCLE('',#8372,0.32);
#3543=CIRCLE('',#8373,0.32);
#3544=CIRCLE('',#8375,0.6);
#3545=CIRCLE('',#8376,0.6);
#4108=VERTEX_POINT('',#12518);
#4109=VERTEX_POINT('',#12520);
#4110=VERTEX_POINT('',#12524);
#4111=VERTEX_POINT('',#12526);
#4991=EDGE_CURVE('',#4108,#4108,#3542,.T.);
#4992=EDGE_CURVE('',#4108,#4109,#2605,.T.);
#4993=EDGE_CURVE('',#4109,#4109,#3543,.T.);
#4994=EDGE_CURVE('',#4110,#4110,#3544,.T.);
#4995=EDGE_CURVE('',#4110,#4111,#2606,.T.);
#4996=EDGE_CURVE('',#4111,#4111,#3545,.T.);
#6737=ORIENTED_EDGE('',*,*,#4991,.F.);
#6738=ORIENTED_EDGE('',*,*,#4992,.T.);
#6739=ORIENTED_EDGE('',*,*,#4993,.T.);
#6740=ORIENTED_EDGE('',*,*,#4992,.F.);
#6741=ORIENTED_EDGE('',*,*,#4994,.F.);
#6742=ORIENTED_EDGE('',*,*,#4995,.T.);
#6743=ORIENTED_EDGE('',*,*,#4996,.T.);
#6744=ORIENTED_EDGE('',*,*,#4995,.F.);
#6745=ORIENTED_EDGE('',*,*,#4994,.T.);
#6746=ORIENTED_EDGE('',*,*,#4991,.T.);
#6747=ORIENTED_EDGE('',*,*,#4996,.F.);
#6748=ORIENTED_EDGE('',*,*,#4993,.F.);
#6966=CYLINDRICAL_SURFACE('',#8371,0.32);
#6967=CYLINDRICAL_SURFACE('',#8374,0.6);
#7321=ADVANCED_FACE('',(#1395),#6966,.F.);
#7322=ADVANCED_FACE('',(#1396),#6967,.T.);
#7323=ADVANCED_FACE('',(#1397,#758),#1022,.T.);
#7324=ADVANCED_FACE('',(#1398,#759),#1023,.F.);
#7393=CLOSED_SHELL('',(#7321,#7322,#7323,#7324));
#8370=AXIS2_PLACEMENT_3D('',#12516,#10402,#10403);
#8371=AXIS2_PLACEMENT_3D('',#12517,#10404,#10405);
#8372=AXIS2_PLACEMENT_3D('',#12519,#10406,#10407);
#8373=AXIS2_PLACEMENT_3D('',#12522,#10409,#10410);
#8374=AXIS2_PLACEMENT_3D('',#12523,#10411,#10412);
#8375=AXIS2_PLACEMENT_3D('',#12525,#10413,#10414);
#8376=AXIS2_PLACEMENT_3D('',#12528,#10416,#10417);
#8377=AXIS2_PLACEMENT_3D('',#12529,#10418,#10419);
#8378=AXIS2_PLACEMENT_3D('',#12530,#10420,#10421);
#10402=DIRECTION('axis',(0.,0.,1.));
#10403=DIRECTION('refdir',(1.,0.,0.));
#10404=DIRECTION('center_axis',(0.,1.,0.));
#10405=DIRECTION('ref_axis',(1.,0.,0.));
#10406=DIRECTION('center_axis',(0.,-1.,0.));
#10407=DIRECTION('ref_axis',(1.,0.,0.));
#10408=DIRECTION('',(0.,-1.,0.));
#10409=DIRECTION('center_axis',(0.,-1.,0.));
#10410=DIRECTION('ref_axis',(1.,0.,0.));
#10411=DIRECTION('center_axis',(0.,1.,0.));
#10412=DIRECTION('ref_axis',(1.,0.,0.));
#10413=DIRECTION('center_axis',(0.,1.,0.));
#10414=DIRECTION('ref_axis',(1.,0.,0.));
#10415=DIRECTION('',(0.,-1.,0.));
#10416=DIRECTION('center_axis',(0.,1.,0.));
#10417=DIRECTION('ref_axis',(1.,0.,0.));
#10418=DIRECTION('center_axis',(0.,1.,0.));
#10419=DIRECTION('ref_axis',(1.,0.,0.));
#10420=DIRECTION('center_axis',(0.,1.,0.));
#10421=DIRECTION('ref_axis',(1.,0.,0.));
#12516=CARTESIAN_POINT('',(0.,0.,0.));
#12517=CARTESIAN_POINT('Origin',(0.,0.,0.));
#12518=CARTESIAN_POINT('',(-0.32,0.16,3.91886975727153E-17));
#12519=CARTESIAN_POINT('Origin',(0.,0.16,0.));
#12520=CARTESIAN_POINT('',(-0.32,0.,3.91886975727153E-17));
#12521=CARTESIAN_POINT('',(-0.32,0.,3.91886975727153E-17));
#12522=CARTESIAN_POINT('Origin',(0.,0.,0.));
#12523=CARTESIAN_POINT('Origin',(0.,0.,0.));
#12524=CARTESIAN_POINT('',(-0.6,0.16,7.34788079488412E-17));
#12525=CARTESIAN_POINT('Origin',(0.,0.16,0.));
#12526=CARTESIAN_POINT('',(-0.6,0.,7.34788079488412E-17));
#12527=CARTESIAN_POINT('',(-0.6,0.,7.34788079488412E-17));
#12528=CARTESIAN_POINT('Origin',(0.,0.,0.));
#12529=CARTESIAN_POINT('Origin',(0.,0.16,0.));
#12530=CARTESIAN_POINT('Origin',(0.,0.,0.));
#12764=UNCERTAINTY_MEASURE_WITH_UNIT(LENGTH_MEASURE(0.001),#12805,
'DISTANCE_ACCURACY_VALUE',
'Maximum model space distance between geometric entities at asserted c
onnectivities');
#12768=UNCERTAINTY_MEASURE_WITH_UNIT(LENGTH_MEASURE(0.001),#12805,
'DISTANCE_ACCURACY_VALUE',
'Maximum model space distance between geometric entities at asserted c
onnectivities');
#12800=(
GEOMETRIC_REPRESENTATION_CONTEXT(3)
GLOBAL_UNCERTAINTY_ASSIGNED_CONTEXT((#12764))
GLOBAL_UNIT_ASSIGNED_CONTEXT((#12805,#12807,#12808))
REPRESENTATION_CONTEXT('','3D')
);
#12804=(
GEOMETRIC_REPRESENTATION_CONTEXT(3)
GLOBAL_UNCERTAINTY_ASSIGNED_CONTEXT((#12768))
GLOBAL_UNIT_ASSIGNED_CONTEXT((#12805,#12807,#12808))
REPRESENTATION_CONTEXT('','3D')
);
#12805=(
LENGTH_UNIT()
NAMED_UNIT(*)
SI_UNIT(.CENTI.,.METRE.)
);
#12807=(
NAMED_UNIT(*)
PLANE_ANGLE_UNIT()
SI_UNIT($,.RADIAN.)
);
#12808=(
NAMED_UNIT(*)
SI_UNIT($,.STERADIAN.)
SOLID_ANGLE_UNIT()
);
#12840=SHAPE_DEFINITION_REPRESENTATION(#12948,#13030);
#12948=PRODUCT_DEFINITION_SHAPE('',$,#13066);
#13030=SHAPE_REPRESENTATION('',(#8370),#12800);
#13034=PRODUCT_DEFINITION_CONTEXT('part definition',#13141,'design');
#13066=PRODUCT_DEFINITION('Flat Washer - M6','Flat Washer - M6',#13101,
#13034);
#13101=PRODUCT_DEFINITION_FORMATION('',$,#13174);
#13141=APPLICATION_CONTEXT(
'Core Data for Automotive Mechanical Design Process');
#13142=PRODUCT_CONTEXT('part definition',#13141,'mechanical');
#13174=PRODUCT('Flat Washer - M6','Flat Washer - M6','Flat Washer - M6',
(#13142));
#13248=COLOUR_RGB('Black',0.12,0.14,0.17);
#13249=FILL_AREA_STYLE_COLOUR('',#13248);
#13250=FILL_AREA_STYLE('',(#13249));
#13251=SURFACE_STYLE_FILL_AREA(#13250);
#13252=SURFACE_SIDE_STYLE('',(#13251));
#13253=SURFACE_STYLE_USAGE(.BOTH.,#13252);
#13254=PRESENTATION_STYLE_ASSIGNMENT((#13253));
ENDSEC;
END-ISO-10303-21;
